ISO-10303-21;
HEADER;
/* Generated by software containing ST-Developer
 * from STEP Tools, Inc. (www.steptools.com) 
 */

FILE_DESCRIPTION(
/* description */ ('STEP AP214'),
/* implementation_level */ '2;1');

FILE_NAME(
/* name */ 'Washer.step',
/* time_stamp */ '2026-11-14T21:32:33-08:00',
/* author */ (''),
/* organization */ (''),
/* preprocessor_version */ 'ST-DEVELOPER v20.2',
/* originating_system */ 'Autodesk Translation Framework v15.17.0.0',
/* authorisation */ '');

FILE_SCHEMA (('AUTOMOTIVE_DESIGN { 1 0 10303 214 3 1 1 }'));
ENDSEC;

DATA;
#10=MECHANICAL_DESIGN_GEOMETRIC_PRESENTATION_REPRESENTATION('',(#182),#10551);
#164=SHAPE_REPRESENTATION_RELATIONSHIP('SRR','None',#10591,#173);
#173=ADVANCED_BREP_SHAPE_REPRESENTATION('',(#192),#10547);
#182=STYLED_ITEM('',(#10644),#192);
#192=MANIFOLD_SOLID_BREP('Body1',#3431);
#282=PLANE('',#3701);
#283=PLANE('',#3707);
#386=FACE_OUTER_BOUND('',#630,.T.);
#387=FACE_OUTER_BOUND('',#631,.T.);
#388=FACE_OUTER_BOUND('',#632,.T.);
#389=FACE_OUTER_BOUND('',#633,.T.);
#390=FACE_OUTER_BOUND('',#634,.T.);
#391=FACE_OUTER_BOUND('',#635,.T.);
#392=FACE_OUTER_BOUND('',#636,.T.);
#393=FACE_OUTER_BOUND('',#637,.T.);
#394=FACE_OUTER_BOUND('',#638,.T.);
#395=FACE_OUTER_BOUND('',#639,.T.);
#630=EDGE_LOOP('',(#2630,#2631,#2632,#2633));
#631=EDGE_LOOP('',(#2634,#2635,#2636,#2637));
#632=EDGE_LOOP('',(#2638,#2639,#2640,#2641));
#633=EDGE_LOOP('',(#2642,#2643,#2644,#2645,#2646,#2647,#2648,#2649));
#634=EDGE_LOOP('',(#2650,#2651,#2652,#2653,#2654,#2655,#2656,#2657));
#635=EDGE_LOOP('',(#2658,#2659,#2660,#2661));
#636=EDGE_LOOP('',(#2662,#2663,#2664,#2665));
#637=EDGE_LOOP('',(#2666,#2667,#2668,#2669));
#638=EDGE_LOOP('',(#2670,#2671,#2672,#2673));
#639=EDGE_LOOP('',(#2674,#2675,#2676,#2677));
#911=LINE('',#7847,#1108);
#912=LINE('',#7850,#1109);
#913=LINE('',#7856,#1110);
#914=LINE('',#7859,#1111);
#915=LINE('',#7864,#1112);
#916=LINE('',#7885,#1113);
#917=LINE('',#7886,#1114);
#918=LINE('',#7889,#1115);
#1108=VECTOR('',#4502,1000.);
#1109=VECTOR('',#4505,1000.);
#1110=VECTOR('',#4510,1000.);
#1111=VECTOR('',#4513,1000.);
#1112=VECTOR('',#4518,1000.);
#1113=VECTOR('',#4547,1000.);
#1114=VECTOR('',#4548,1000.);
#1115=VECTOR('',#4553,1000.);
#1216=CIRCLE('',#3693,1.1);
#1217=CIRCLE('',#3694,1.1);
#1218=CIRCLE('',#3696,1.7);
#1219=CIRCLE('',#3697,1.7);
#1220=CIRCLE('',#3699,5.);
#1221=CIRCLE('',#3700,5.);
#1222=CIRCLE('',#3702,6.);
#1223=CIRCLE('',#3703,1.1);
#1224=CIRCLE('',#3704,6.);
#1225=CIRCLE('',#3705,1.7);
#1226=CIRCLE('',#3706,1.5);
#1227=CIRCLE('',#3708,1.1);
#1228=CIRCLE('',#3709,6.);
#1229=CIRCLE('',#3710,1.5);
#1230=CIRCLE('',#3711,1.7);
#1231=CIRCLE('',#3712,6.);
#1568=VERTEX_POINT('',#7843);
#1569=VERTEX_POINT('',#7844);
#1570=VERTEX_POINT('',#7846);
#1571=VERTEX_POINT('',#7848);
#1572=VERTEX_POINT('',#7852);
#1573=VERTEX_POINT('',#7853);
#1574=VERTEX_POINT('',#7855);
#1575=VERTEX_POINT('',#7857);
#1576=VERTEX_POINT('',#7861);
#1577=VERTEX_POINT('',#7863);
#1578=VERTEX_POINT('',#7867);
#1579=VERTEX_POINT('',#7870);
#1580=VERTEX_POINT('',#7872);
#1581=VERTEX_POINT('',#7876);
#1582=VERTEX_POINT('',#7879);
#1583=VERTEX_POINT('',#7881);
#1928=EDGE_CURVE('',#1568,#1569,#1216,.T.);
#1929=EDGE_CURVE('',#1570,#1568,#911,.T.);
#1930=EDGE_CURVE('',#1571,#1570,#1217,.T.);
#1931=EDGE_CURVE('',#1569,#1571,#912,.T.);
#1932=EDGE_CURVE('',#1572,#1573,#1218,.T.);
#1933=EDGE_CURVE('',#1573,#1574,#913,.T.);
#1934=EDGE_CURVE('',#1574,#1575,#1219,.T.);
#1935=EDGE_CURVE('',#1572,#1575,#914,.T.);
#1936=EDGE_CURVE('',#1576,#1571,#1220,.T.);
#1937=EDGE_CURVE('',#1576,#1577,#915,.T.);
#1938=EDGE_CURVE('',#1577,#1569,#1221,.T.);
#1939=EDGE_CURVE('',#1578,#1574,#1222,.T.);
#1940=EDGE_CURVE('',#1578,#1576,#1223,.T.);
#1941=EDGE_CURVE('',#1579,#1570,#1224,.T.);
#1942=EDGE_CURVE('',#1580,#1579,#1225,.T.);
#1943=EDGE_CURVE('',#1575,#1580,#1226,.T.);
#1944=EDGE_CURVE('',#1577,#1581,#1227,.T.);
#1945=EDGE_CURVE('',#1573,#1581,#1228,.T.);
#1946=EDGE_CURVE('',#1582,#1572,#1229,.T.);
#1947=EDGE_CURVE('',#1583,#1582,#1230,.T.);
#1948=EDGE_CURVE('',#1568,#1583,#1231,.T.);
#1949=EDGE_CURVE('',#1582,#1580,#916,.T.);
#1950=EDGE_CURVE('',#1583,#1579,#917,.T.);
#1951=EDGE_CURVE('',#1581,#1578,#918,.T.);
#2630=ORIENTED_EDGE('',*,*,#1928,.F.);
#2631=ORIENTED_EDGE('',*,*,#1929,.F.);
#2632=ORIENTED_EDGE('',*,*,#1930,.F.);
#2633=ORIENTED_EDGE('',*,*,#1931,.F.);
#2634=ORIENTED_EDGE('',*,*,#1932,.T.);
#2635=ORIENTED_EDGE('',*,*,#1933,.T.);
#2636=ORIENTED_EDGE('',*,*,#1934,.T.);
#2637=ORIENTED_EDGE('',*,*,#1935,.F.);
#2638=ORIENTED_EDGE('',*,*,#1936,.F.);
#2639=ORIENTED_EDGE('',*,*,#1937,.T.);
#2640=ORIENTED_EDGE('',*,*,#1938,.T.);
#2641=ORIENTED_EDGE('',*,*,#1931,.T.);
#2642=ORIENTED_EDGE('',*,*,#1939,.F.);
#2643=ORIENTED_EDGE('',*,*,#1940,.T.);
#2644=ORIENTED_EDGE('',*,*,#1936,.T.);
#2645=ORIENTED_EDGE('',*,*,#1930,.T.);
#2646=ORIENTED_EDGE('',*,*,#1941,.F.);
#2647=ORIENTED_EDGE('',*,*,#1942,.F.);
#2648=ORIENTED_EDGE('',*,*,#1943,.F.);
#2649=ORIENTED_EDGE('',*,*,#1934,.F.);
#2650=ORIENTED_EDGE('',*,*,#1938,.F.);
#2651=ORIENTED_EDGE('',*,*,#1944,.T.);
#2652=ORIENTED_EDGE('',*,*,#1945,.F.);
#2653=ORIENTED_EDGE('',*,*,#1932,.F.);
#2654=ORIENTED_EDGE('',*,*,#1946,.F.);
#2655=ORIENTED_EDGE('',*,*,#1947,.F.);
#2656=ORIENTED_EDGE('',*,*,#1948,.F.);
#2657=ORIENTED_EDGE('',*,*,#1928,.T.);
#2658=ORIENTED_EDGE('',*,*,#1947,.T.);
#2659=ORIENTED_EDGE('',*,*,#1949,.T.);
#2660=ORIENTED_EDGE('',*,*,#1942,.T.);
#2661=ORIENTED_EDGE('',*,*,#1950,.F.);
#2662=ORIENTED_EDGE('',*,*,#1946,.T.);
#2663=ORIENTED_EDGE('',*,*,#1935,.T.);
#2664=ORIENTED_EDGE('',*,*,#1943,.T.);
#2665=ORIENTED_EDGE('',*,*,#1949,.F.);
#2666=ORIENTED_EDGE('',*,*,#1945,.T.);
#2667=ORIENTED_EDGE('',*,*,#1951,.T.);
#2668=ORIENTED_EDGE('',*,*,#1939,.T.);
#2669=ORIENTED_EDGE('',*,*,#1933,.F.);
#2670=ORIENTED_EDGE('',*,*,#1941,.T.);
#2671=ORIENTED_EDGE('',*,*,#1929,.T.);
#2672=ORIENTED_EDGE('',*,*,#1948,.T.);
#2673=ORIENTED_EDGE('',*,*,#1950,.T.);
#2674=ORIENTED_EDGE('',*,*,#1944,.F.);
#2675=ORIENTED_EDGE('',*,*,#1937,.F.);
#2676=ORIENTED_EDGE('',*,*,#1940,.F.);
#2677=ORIENTED_EDGE('',*,*,#1951,.F.);
#3178=CYLINDRICAL_SURFACE('',#3692,1.1);
#3179=CYLINDRICAL_SURFACE('',#3695,1.7);
#3180=CYLINDRICAL_SURFACE('',#3698,5.);
#3181=CYLINDRICAL_SURFACE('',#3713,1.7);
#3182=CYLINDRICAL_SURFACE('',#3714,1.5);
#3183=CYLINDRICAL_SURFACE('',#3715,6.);
#3184=CYLINDRICAL_SURFACE('',#3716,6.);
#3185=CYLINDRICAL_SURFACE('',#3717,1.1);
#3298=ADVANCED_FACE('',(#386),#3178,.T.);
#3299=ADVANCED_FACE('',(#387),#3179,.F.);
#3300=ADVANCED_FACE('',(#388),#3180,.T.);
#3301=ADVANCED_FACE('',(#389),#282,.T.);
#3302=ADVANCED_FACE('',(#390),#283,.F.);
#3303=ADVANCED_FACE('',(#391),#3181,.F.);
#3304=ADVANCED_FACE('',(#392),#3182,.T.);
#3305=ADVANCED_FACE('',(#393),#3183,.T.);
#3306=ADVANCED_FACE('',(#394),#3184,.T.);
#3307=ADVANCED_FACE('',(#395),#3185,.T.);
#3431=CLOSED_SHELL('',(#3298,#3299,#3300,#3301,#3302,#3303,#3304,#3305,
#3306,#3307));
#3691=AXIS2_PLACEMENT_3D('',#7841,#4496,#4497);
#3692=AXIS2_PLACEMENT_3D('',#7842,#4498,#4499);
#3693=AXIS2_PLACEMENT_3D('',#7845,#4500,#4501);
#3694=AXIS2_PLACEMENT_3D('',#7849,#4503,#4504);
#3695=AXIS2_PLACEMENT_3D('',#7851,#4506,#4507);
#3696=AXIS2_PLACEMENT_3D('',#7854,#4508,#4509);
#3697=AXIS2_PLACEMENT_3D('',#7858,#4511,#4512);
#3698=AXIS2_PLACEMENT_3D('',#7860,#4514,#4515);
#3699=AXIS2_PLACEMENT_3D('',#7862,#4516,#4517);
#3700=AXIS2_PLACEMENT_3D('',#7865,#4519,#4520);
#3701=AXIS2_PLACEMENT_3D('',#7866,#4521,#4522);
#3702=AXIS2_PLACEMENT_3D('',#7868,#4523,#4524);
#3703=AXIS2_PLACEMENT_3D('',#7869,#4525,#4526);
#3704=AXIS2_PLACEMENT_3D('',#7871,#4527,#4528);
#3705=AXIS2_PLACEMENT_3D('',#7873,#4529,#4530);
#3706=AXIS2_PLACEMENT_3D('',#7874,#4531,#4532);
#3707=AXIS2_PLACEMENT_3D('',#7875,#4533,#4534);
#3708=AXIS2_PLACEMENT_3D('',#7877,#4535,#4536);
#3709=AXIS2_PLACEMENT_3D('',#7878,#4537,#4538);
#3710=AXIS2_PLACEMENT_3D('',#7880,#4539,#4540);
#3711=AXIS2_PLACEMENT_3D('',#7882,#4541,#4542);
#3712=AXIS2_PLACEMENT_3D('',#7883,#4543,#4544);
#3713=AXIS2_PLACEMENT_3D('',#7884,#4545,#4546);
#3714=AXIS2_PLACEMENT_3D('',#7887,#4549,#4550);
#3715=AXIS2_PLACEMENT_3D('',#7888,#4551,#4552);
#3716=AXIS2_PLACEMENT_3D('',#7890,#4554,#4555);
#3717=AXIS2_PLACEMENT_3D('',#7891,#4556,#4557);
#4496=DIRECTION('axis',(0.,0.,1.));
#4497=DIRECTION('refdir',(1.,0.,0.));
#4498=DIRECTION('center_axis',(0.,0.,1.));
#4499=DIRECTION('ref_axis',(1.,0.,0.));
#4500=DIRECTION('center_axis',(0.,0.,-1.));
#4501=DIRECTION('ref_axis',(1.,0.,0.));
#4502=DIRECTION('',(0.,0.,-1.));
#4503=DIRECTION('center_axis',(0.,0.,1.));
#4504=DIRECTION('ref_axis',(1.,0.,0.));
#4505=DIRECTION('',(0.,0.,1.));
#4506=DIRECTION('center_axis',(0.,0.,1.));
#4507=DIRECTION('ref_axis',(1.,0.,0.));
#4508=DIRECTION('center_axis',(0.,0.,-1.));
#4509=DIRECTION('ref_axis',(1.,-1.78574475468201E-15,0.));
#4510=DIRECTION('',(0.,0.,1.));
#4511=DIRECTION('center_axis',(0.,0.,1.));
#4512=DIRECTION('ref_axis',(-1.,0.,0.));
#4513=DIRECTION('',(0.,0.,1.));
#4514=DIRECTION('center_axis',(0.,0.,-1.));
#4515=DIRECTION('ref_axis',(-5.0532154980743E-16,1.,0.));
#4516=DIRECTION('center_axis',(0.,0.,1.));
#4517=DIRECTION('ref_axis',(1.,0.,0.));
#4518=DIRECTION('',(0.,0.,-1.));
#4519=DIRECTION('center_axis',(0.,0.,1.));
#4520=DIRECTION('ref_axis',(1.,0.,0.));
#4521=DIRECTION('center_axis',(0.,0.,1.));
#4522=DIRECTION('ref_axis',(1.,0.,0.));
#4523=DIRECTION('center_axis',(0.,0.,-1.));
#4524=DIRECTION('ref_axis',(1.,0.,0.));
#4525=DIRECTION('center_axis',(0.,0.,1.));
#4526=DIRECTION('ref_axis',(1.,0.,0.));
#4527=DIRECTION('center_axis',(0.,0.,-1.));
#4528=DIRECTION('ref_axis',(-1.,0.,0.));
#4529=DIRECTION('center_axis',(0.,0.,1.));
#4530=DIRECTION('ref_axis',(1.,0.,0.));
#4531=DIRECTION('center_axis',(0.,0.,-1.));
#4532=DIRECTION('ref_axis',(1.,0.,0.));
#4533=DIRECTION('center_axis',(0.,0.,1.));
#4534=DIRECTION('ref_axis',(1.,0.,0.));
#4535=DIRECTION('center_axis',(0.,0.,-1.));
#4536=DIRECTION('ref_axis',(1.,0.,0.));
#4537=DIRECTION('center_axis',(0.,0.,1.));
#4538=DIRECTION('ref_axis',(1.,0.,0.));
#4539=DIRECTION('center_axis',(0.,0.,1.));
#4540=DIRECTION('ref_axis',(1.,0.,0.));
#4541=DIRECTION('center_axis',(0.,0.,-1.));
#4542=DIRECTION('ref_axis',(1.,1.78574475468201E-15,0.));
#4543=DIRECTION('center_axis',(0.,0.,1.));
#4544=DIRECTION('ref_axis',(1.,0.,0.));
#4545=DIRECTION('center_axis',(0.,0.,1.));
#4546=DIRECTION('ref_axis',(-0.791487217192215,0.61118572056399,0.));
#4547=DIRECTION('',(0.,0.,1.));
#4548=DIRECTION('',(0.,0.,1.));
#4549=DIRECTION('center_axis',(0.,0.,1.));
#4550=DIRECTION('ref_axis',(1.,0.,0.));
#4551=DIRECTION('center_axis',(0.,0.,1.));
#4552=DIRECTION('ref_axis',(1.,0.,0.));
#4553=DIRECTION('',(0.,0.,1.));
#4554=DIRECTION('center_axis',(0.,0.,1.));
#4555=DIRECTION('ref_axis',(1.,0.,0.));
#4556=DIRECTION('center_axis',(0.,0.,1.));
#4557=DIRECTION('ref_axis',(-0.504127969118338,-0.863628965906436,0.));
#7841=CARTESIAN_POINT('',(0.,0.,0.));
#7842=CARTESIAN_POINT('Origin',(-2.51665162595684,-2.97933962373691,-0.00100000000000002));
#7843=CARTESIAN_POINT('',(-1.43590173451363,-2.77445020930684,0.));
#7844=CARTESIAN_POINT('',(-3.22647644353441,-3.81966618427809,0.));
#7845=CARTESIAN_POINT('Origin',(-2.51665162595684,-2.97933962373691,0.));
#7846=CARTESIAN_POINT('',(-1.43590173451363,-2.77445020930684,0.7));
#7847=CARTESIAN_POINT('',(-1.43590173451363,-2.77445020930684,-0.00100000000000002));
#7848=CARTESIAN_POINT('',(-3.22647644353441,-3.81966618427809,0.7));
#7849=CARTESIAN_POINT('Origin',(-2.51665162595684,-2.97933962373691,0.7));
#7850=CARTESIAN_POINT('',(-3.22647644353441,-3.81966618427809,0.7));
#7851=CARTESIAN_POINT('Origin',(1.2766327138965,0.865684251173834,-0.00100000000000002));
#7852=CARTESIAN_POINT('',(0.598421584638982,2.42453949273773,0.));
#7853=CARTESIAN_POINT('',(2.61328937992658,-0.18471993634512,0.));
#7854=CARTESIAN_POINT('Origin',(1.2766327138965,0.865684251173834,0.));
#7855=CARTESIAN_POINT('',(2.61328937992658,-0.18471993634512,0.7));
#7856=CARTESIAN_POINT('',(2.61328937992658,-0.18471993634512,-0.00100000000000002));
#7857=CARTESIAN_POINT('',(0.598421584638982,2.42453949273773,0.7));
#7858=CARTESIAN_POINT('Origin',(1.2766327138965,0.865684251173834,0.7));
#7859=CARTESIAN_POINT('',(0.598421584638982,2.42453949273773,-0.00100000000000002));
#7860=CARTESIAN_POINT('Origin',(0.,0.,0.7));
#7861=CARTESIAN_POINT('',(3.22647644353441,-3.81966618427809,0.7));
#7862=CARTESIAN_POINT('Origin',(0.,0.,0.7));
#7863=CARTESIAN_POINT('',(3.22647644353441,-3.81966618427809,0.));
#7864=CARTESIAN_POINT('',(3.22647644353441,-3.81966618427809,0.7));
#7865=CARTESIAN_POINT('Origin',(0.,0.,0.));
#7866=CARTESIAN_POINT('Origin',(0.,0.,0.7));
#7867=CARTESIAN_POINT('',(1.43590173451363,-2.77445020930684,0.7));
#7868=CARTESIAN_POINT('Origin',(7.33090114238568,-3.89202883347084,0.7));
#7869=CARTESIAN_POINT('Origin',(2.51665162595684,-2.97933962373691,0.7));
#7870=CARTESIAN_POINT('',(-2.61328937992658,-0.18471993634512,0.7));
#7871=CARTESIAN_POINT('Origin',(-7.33090114238567,-3.89202883347085,0.7));
#7872=CARTESIAN_POINT('',(-0.598421584638982,2.42453949273774,0.7));
#7873=CARTESIAN_POINT('Origin',(-1.2766327138965,0.865684251173833,0.7));
#7874=CARTESIAN_POINT('Origin',(0.,3.8,0.7));
#7875=CARTESIAN_POINT('Origin',(0.,0.,0.));
#7876=CARTESIAN_POINT('',(1.43590173451363,-2.77445020930684,0.));
#7877=CARTESIAN_POINT('Origin',(2.51665162595684,-2.97933962373691,0.));
#7878=CARTESIAN_POINT('Origin',(7.33090114238568,-3.89202883347084,0.));
#7879=CARTESIAN_POINT('',(-0.598421584638982,2.42453949273774,0.));
#7880=CARTESIAN_POINT('Origin',(0.,3.8,0.));
#7881=CARTESIAN_POINT('',(-2.61328937992658,-0.18471993634512,0.));
#7882=CARTESIAN_POINT('Origin',(-1.2766327138965,0.865684251173833,0.));
#7883=CARTESIAN_POINT('Origin',(-7.33090114238567,-3.89202883347085,0.));
#7884=CARTESIAN_POINT('Origin',(-1.2766327138965,0.865684251173833,-0.00100000000000002));
#7885=CARTESIAN_POINT('',(-0.598421584638982,2.42453949273774,-0.00100000000000002));
#7886=CARTESIAN_POINT('',(-2.61328937992658,-0.18471993634512,-0.00100000000000002));
#7887=CARTESIAN_POINT('Origin',(0.,3.8,-0.00100000000000002));
#7888=CARTESIAN_POINT('Origin',(7.33090114238568,-3.89202883347084,-0.00100000000000002));
#7889=CARTESIAN_POINT('',(1.43590173451363,-2.77445020930684,-0.00100000000000002));
#7890=CARTESIAN_POINT('Origin',(-7.33090114238567,-3.89202883347085,-0.00100000000000002));
#7891=CARTESIAN_POINT('Origin',(2.51665162595684,-2.97933962373691,0.7));
#10536=UNCERTAINTY_MEASURE_WITH_UNIT(LENGTH_MEASURE(0.01),#10552,
'DISTANCE_ACCURACY_VALUE',
'Maximum model space distance between geometric entities at asserted c
onnectivities');
#10540=UNCERTAINTY_MEASURE_WITH_UNIT(LENGTH_MEASURE(0.01),#10552,
'DISTANCE_ACCURACY_VALUE',
'Maximum model space distance between geometric entities at asserted c
onnectivities');
#10547=(
GEOMETRIC_REPRESENTATION_CONTEXT(3)
GLOBAL_UNCERTAINTY_ASSIGNED_CONTEXT((#10536))
GLOBAL_UNIT_ASSIGNED_CONTEXT((#10552,#10554,#10555))
REPRESENTATION_CONTEXT('','3D')
);
#10551=(
GEOMETRIC_REPRESENTATION_CONTEXT(3)
GLOBAL_UNCERTAINTY_ASSIGNED_CONTEXT((#10540))
GLOBAL_UNIT_ASSIGNED_CONTEXT((#10552,#10554,#10555))
REPRESENTATION_CONTEXT('','3D')
);
#10552=(
LENGTH_UNIT()
NAMED_UNIT(*)
SI_UNIT(.MILLI.,.METRE.)
);
#10554=(
NAMED_UNIT(*)
PLANE_ANGLE_UNIT()
SI_UNIT($,.RADIAN.)
);
#10555=(
NAMED_UNIT(*)
SI_UNIT($,.STERADIAN.)
SOLID_ANGLE_UNIT()
);
#10562=SHAPE_DEFINITION_REPRESENTATION(#10572,#10591);
#10572=PRODUCT_DEFINITION_SHAPE('',$,#10602);
#10591=SHAPE_REPRESENTATION('',(#3691),#10547);
#10595=PRODUCT_DEFINITION_CONTEXT('part definition',#10627,'design');
#10602=PRODUCT_DEFINITION('Washer','Washer',#10612,#10595);
#10612=PRODUCT_DEFINITION_FORMATION('',$,#10635);
#10627=APPLICATION_CONTEXT(
'Core Data for Automotive Mechanical Design Process');
#10628=PRODUCT_CONTEXT('part definition',#10627,'mechanical');
#10635=PRODUCT('Washer','Washer',$,(#10628));
#10644=PRESENTATION_STYLE_ASSIGNMENT((#10651));
#10651=SURFACE_STYLE_USAGE(.BOTH.,#10658);
#10658=SURFACE_SIDE_STYLE('',(#10665));
#10665=SURFACE_STYLE_FILL_AREA(#10672);
#10672=FILL_AREA_STYLE('Opaque(31,36,43)',(#10679));
#10679=FILL_AREA_STYLE_COLOUR('Opaque(31,36,43)',#10686);
#10686=COLOUR_RGB('Opaque(31,36,43)',0.12156862745098,0.141176470588235,
0.168627450980392);
ENDSEC;
END-ISO-10303-21;
